ISO-10303-21;
HEADER;
/* Generated by software containing ST-Developer
 * from STEP Tools, Inc. (www.steptools.com) 
 */

FILE_DESCRIPTION(
/* description */ ('PAT-091'),
/* implementation_level */ '2;1');

FILE_NAME(
/* name */ 'Axle distance sleeve 5 mm (7).step',
/* time_stamp */ '2026-10-27T15:34:44-07:00',
/* author */ (''),
/* organization */ (''),
/* preprocessor_version */ 'ST-DEVELOPER v20.2',
/* originating_system */ 'Autodesk Translation Framework v15.17.0.0',
/* authorisation */ '');

FILE_SCHEMA (('AUTOMOTIVE_DESIGN { 1 0 10303 214 3 1 1 }'));
ENDSEC;

DATA;
#10=MECHANICAL_DESIGN_GEOMETRIC_PRESENTATION_REPRESENTATION('',(#1020),#25100);
#800=SHAPE_REPRESENTATION_RELATIONSHIP('SRR','None',#25564,#910);
#910=ADVANCED_BREP_SHAPE_REPRESENTATION('',(#1142),#25034);
#1020=STYLED_ITEM('',(#26191),#1142);
#1142=MANIFOLD_SOLID_BREP('Body1',#13299);
#1464=FACE_BOUND('',#3529,.T.);
#1465=FACE_BOUND('',#3531,.T.);
#1861=PLANE('',#15389);
#1862=PLANE('',#15390);
#2459=FACE_OUTER_BOUND('',#3526,.T.);
#2460=FACE_OUTER_BOUND('',#3527,.T.);
#2461=FACE_OUTER_BOUND('',#3528,.T.);
#2462=FACE_OUTER_BOUND('',#3530,.T.);
#3526=EDGE_LOOP('',(#10584,#10585,#10586,#10587));
#3527=EDGE_LOOP('',(#10588,#10589,#10590,#10591));
#3528=EDGE_LOOP('',(#10592));
#3529=EDGE_LOOP('',(#10593));
#3530=EDGE_LOOP('',(#10594));
#3531=EDGE_LOOP('',(#10595));
#4579=LINE('',#22822,#5319);
#4580=LINE('',#22828,#5320);
#5319=VECTOR('',#18523,0.604999999999997);
#5320=VECTOR('',#18530,0.799999999999997);
#5951=CIRCLE('',#15384,0.604999999999997);
#5952=CIRCLE('',#15385,0.604999999999997);
#5953=CIRCLE('',#15387,0.799999999999997);
#5954=CIRCLE('',#15388,0.799999999999997);
#6918=VERTEX_POINT('',#22819);
#6919=VERTEX_POINT('',#22821);
#6920=VERTEX_POINT('',#22825);
#6921=VERTEX_POINT('',#22827);
#8227=EDGE_CURVE('',#6918,#6918,#5951,.T.);
#8228=EDGE_CURVE('',#6918,#6919,#4579,.T.);
#8229=EDGE_CURVE('',#6919,#6919,#5952,.T.);
#8230=EDGE_CURVE('',#6920,#6920,#5953,.T.);
#8231=EDGE_CURVE('',#6920,#6921,#4580,.T.);
#8232=EDGE_CURVE('',#6921,#6921,#5954,.T.);
#10584=ORIENTED_EDGE('',*,*,#8227,.F.);
#10585=ORIENTED_EDGE('',*,*,#8228,.T.);
#10586=ORIENTED_EDGE('',*,*,#8229,.T.);
#10587=ORIENTED_EDGE('',*,*,#8228,.F.);
#10588=ORIENTED_EDGE('',*,*,#8230,.F.);
#10589=ORIENTED_EDGE('',*,*,#8231,.T.);
#10590=ORIENTED_EDGE('',*,*,#8232,.T.);
#10591=ORIENTED_EDGE('',*,*,#8231,.F.);
#10592=ORIENTED_EDGE('',*,*,#8230,.T.);
#10593=ORIENTED_EDGE('',*,*,#8227,.T.);
#10594=ORIENTED_EDGE('',*,*,#8232,.F.);
#10595=ORIENTED_EDGE('',*,*,#8229,.F.);
#12242=CYLINDRICAL_SURFACE('',#15383,0.604999999999997);
#12243=CYLINDRICAL_SURFACE('',#15386,0.799999999999997);
#12826=ADVANCED_FACE('',(#2459),#12242,.F.);
#12827=ADVANCED_FACE('',(#2460),#12243,.T.);
#12828=ADVANCED_FACE('',(#2461,#1464),#1861,.T.);
#12829=ADVANCED_FACE('',(#2462,#1465),#1862,.F.);
#13299=CLOSED_SHELL('',(#12826,#12827,#12828,#12829));
#15382=AXIS2_PLACEMENT_3D('',#22817,#18517,#18518);
#15383=AXIS2_PLACEMENT_3D('',#22818,#18519,#18520);
#15384=AXIS2_PLACEMENT_3D('',#22820,#18521,#18522);
#15385=AXIS2_PLACEMENT_3D('',#22823,#18524,#18525);
#15386=AXIS2_PLACEMENT_3D('',#22824,#18526,#18527);
#15387=AXIS2_PLACEMENT_3D('',#22826,#18528,#18529);
#15388=AXIS2_PLACEMENT_3D('',#22829,#18531,#18532);
#15389=AXIS2_PLACEMENT_3D('',#22830,#18533,#18534);
#15390=AXIS2_PLACEMENT_3D('',#22831,#18535,#18536);
#18517=DIRECTION('axis',(0.,0.,1.));
#18518=DIRECTION('refdir',(1.,0.,0.));
#18519=DIRECTION('center_axis',(0.,1.,0.));
#18520=DIRECTION('ref_axis',(1.,0.,0.));
#18521=DIRECTION('center_axis',(0.,-1.,0.));
#18522=DIRECTION('ref_axis',(1.,0.,0.));
#18523=DIRECTION('',(0.,-1.,0.));
#18524=DIRECTION('center_axis',(0.,-1.,0.));
#18525=DIRECTION('ref_axis',(1.,0.,0.));
#18526=DIRECTION('center_axis',(0.,1.,0.));
#18527=DIRECTION('ref_axis',(1.,0.,0.));
#18528=DIRECTION('center_axis',(0.,1.,0.));
#18529=DIRECTION('ref_axis',(1.,0.,0.));
#18530=DIRECTION('',(0.,-1.,0.));
#18531=DIRECTION('center_axis',(0.,1.,0.));
#18532=DIRECTION('ref_axis',(1.,0.,0.));
#18533=DIRECTION('center_axis',(0.,1.,0.));
#18534=DIRECTION('ref_axis',(1.,0.,0.));
#18535=DIRECTION('center_axis',(0.,1.,0.));
#18536=DIRECTION('ref_axis',(1.,0.,0.));
#22817=CARTESIAN_POINT('',(0.,0.,0.));
#22818=CARTESIAN_POINT('Origin',(38.7298334620742,-7.5,13.));
#22819=CARTESIAN_POINT('',(38.1248334620742,-7.,13.));
#22820=CARTESIAN_POINT('Origin',(38.7298334620742,-7.,13.));
#22821=CARTESIAN_POINT('',(38.1248334620742,-7.5,13.));
#22822=CARTESIAN_POINT('',(38.1248334620742,-7.5,13.));
#22823=CARTESIAN_POINT('Origin',(38.7298334620742,-7.5,13.));
#22824=CARTESIAN_POINT('Origin',(38.7298334620742,-7.5,13.));
#22825=CARTESIAN_POINT('',(37.9298334620742,-7.,13.));
#22826=CARTESIAN_POINT('Origin',(38.7298334620742,-7.,13.));
#22827=CARTESIAN_POINT('',(37.9298334620742,-7.5,13.));
#22828=CARTESIAN_POINT('',(37.9298334620742,-7.5,13.));
#22829=CARTESIAN_POINT('Origin',(38.7298334620742,-7.5,13.));
#22830=CARTESIAN_POINT('Origin',(38.7298334620742,-7.,13.));
#22831=CARTESIAN_POINT('Origin',(38.7298334620742,-7.5,13.));
#24913=UNCERTAINTY_MEASURE_WITH_UNIT(LENGTH_MEASURE(0.001),#25101,
'DISTANCE_ACCURACY_VALUE',
'Maximum model space distance between geometric entities at asserted c
onnectivities');
#24979=UNCERTAINTY_MEASURE_WITH_UNIT(LENGTH_MEASURE(0.001),#25101,
'DISTANCE_ACCURACY_VALUE',
'Maximum model space distance between geometric entities at asserted c
onnectivities');
#25034=(
GEOMETRIC_REPRESENTATION_CONTEXT(3)
GLOBAL_UNCERTAINTY_ASSIGNED_CONTEXT((#24913))
GLOBAL_UNIT_ASSIGNED_CONTEXT((#25101,#25103,#25104))
REPRESENTATION_CONTEXT('','3D')
);
#25100=(
GEOMETRIC_REPRESENTATION_CONTEXT(3)
GLOBAL_UNCERTAINTY_ASSIGNED_CONTEXT((#24979))
GLOBAL_UNIT_ASSIGNED_CONTEXT((#25101,#25103,#25104))
REPRESENTATION_CONTEXT('','3D')
);
#25101=(
LENGTH_UNIT()
NAMED_UNIT(*)
SI_UNIT(.CENTI.,.METRE.)
);
#25103=(
NAMED_UNIT(*)
PLANE_ANGLE_UNIT()
SI_UNIT($,.RADIAN.)
);
#25104=(
NAMED_UNIT(*)
SI_UNIT($,.STERADIAN.)
SOLID_ANGLE_UNIT()
);
#25159=SHAPE_DEFINITION_REPRESENTATION(#25279,#25564);
#25279=PRODUCT_DEFINITION_SHAPE('',$,#25685);
#25564=SHAPE_REPRESENTATION('',(#15382),#25034);
#25630=PRODUCT_DEFINITION_CONTEXT('part definition',#25992,'design');
#25685=PRODUCT_DEFINITION('Axle distance sleeve 5 mm (7)',
'Axle distance sleeve 5 mm (7)',#25805,#25630);
#25805=PRODUCT_DEFINITION_FORMATION('',$,#26048);
#25992=APPLICATION_CONTEXT(
'Core Data for Automotive Mechanical Design Process');
#25993=PRODUCT_CONTEXT('part definition',#25992,'mechanical');
#26048=PRODUCT('Axle distance sleeve 5 mm (7)',
'Axle distance sleeve 5 mm (7)','Axle distance sleeve 5 mm (7)',(#25993));
#26185=COLOUR_RGB('Grey',0.48,0.52,0.57);
#26186=FILL_AREA_STYLE_COLOUR('',#26185);
#26187=FILL_AREA_STYLE('',(#26186));
#26188=SURFACE_STYLE_FILL_AREA(#26187);
#26189=SURFACE_SIDE_STYLE('',(#26188));
#26190=SURFACE_STYLE_USAGE(.BOTH.,#26189);
#26191=PRESENTATION_STYLE_ASSIGNMENT((#26190));
ENDSEC;
END-ISO-10303-21;
